ISO-10303-21;
HEADER;
/* Generated by software containing ST-Developer
 * from STEP Tools, Inc. (www.steptools.com) 
 */

FILE_DESCRIPTION(
/* description */ ('PAT-091'),
/* implementation_level */ '2;1');

FILE_NAME(
/* name */ 'M4 low-profile retaining screw (14).step',
/* time_stamp */ '2026-10-27T15:34:44-07:00',
/* author */ (''),
/* organization */ (''),
/* preprocessor_version */ 'ST-DEVELOPER v20.2',
/* originating_system */ 'Autodesk Translation Framework v15.17.0.0',
/* authorisation */ '');

FILE_SCHEMA (('AUTOMOTIVE_DESIGN { 1 0 10303 214 3 1 1 }'));
ENDSEC;

DATA;
#10=MECHANICAL_DESIGN_GEOMETRIC_PRESENTATION_REPRESENTATION('',(#1068),#25100);
#848=SHAPE_REPRESENTATION_RELATIONSHIP('SRR','None',#25615,#958);
#958=ADVANCED_BREP_SHAPE_REPRESENTATION('',(#1189),#25085);
#1068=STYLED_ITEM('',(#26198),#1189);
#1189=MANIFOLD_SOLID_BREP('Body1',#13348);
#1615=FACE_BOUND('',#3984,.T.);
#2018=PLANE('',#16113);
#2019=PLANE('',#16118);
#2020=PLANE('',#16121);
#2765=FACE_OUTER_BOUND('',#3983,.T.);
#2766=FACE_OUTER_BOUND('',#3985,.T.);
#2767=FACE_OUTER_BOUND('',#3986,.T.);
#2768=FACE_OUTER_BOUND('',#3987,.T.);
#2769=FACE_OUTER_BOUND('',#3988,.T.);
#3983=EDGE_LOOP('',(#11684));
#3984=EDGE_LOOP('',(#11685));
#3985=EDGE_LOOP('',(#11686,#11687,#11688,#11689));
#3986=EDGE_LOOP('',(#11690));
#3987=EDGE_LOOP('',(#11691,#11692,#11693,#11694));
#3988=EDGE_LOOP('',(#11695));
#4830=LINE('',#24172,#5570);
#4831=LINE('',#24176,#5571);
#5570=VECTOR('',#20240,0.350000000000001);
#5571=VECTOR('',#20245,0.199999999999999);
#6250=CIRCLE('',#16114,0.350000000000001);
#6251=CIRCLE('',#16115,0.199999999999999);
#6252=CIRCLE('',#16117,0.350000000000001);
#6253=CIRCLE('',#16120,0.199999999999999);
#7283=VERTEX_POINT('',#24165);
#7284=VERTEX_POINT('',#24167);
#7285=VERTEX_POINT('',#24170);
#7286=VERTEX_POINT('',#24175);
#8777=EDGE_CURVE('',#7283,#7283,#6250,.T.);
#8778=EDGE_CURVE('',#7284,#7284,#6251,.T.);
#8779=EDGE_CURVE('',#7285,#7285,#6252,.T.);
#8780=EDGE_CURVE('',#7285,#7283,#4830,.T.);
#8781=EDGE_CURVE('',#7284,#7286,#4831,.T.);
#8782=EDGE_CURVE('',#7286,#7286,#6253,.T.);
#11684=ORIENTED_EDGE('',*,*,#8777,.F.);
#11685=ORIENTED_EDGE('',*,*,#8778,.T.);
#11686=ORIENTED_EDGE('',*,*,#8779,.F.);
#11687=ORIENTED_EDGE('',*,*,#8780,.T.);
#11688=ORIENTED_EDGE('',*,*,#8777,.T.);
#11689=ORIENTED_EDGE('',*,*,#8780,.F.);
#11690=ORIENTED_EDGE('',*,*,#8779,.T.);
#11691=ORIENTED_EDGE('',*,*,#8778,.F.);
#11692=ORIENTED_EDGE('',*,*,#8781,.T.);
#11693=ORIENTED_EDGE('',*,*,#8782,.T.);
#11694=ORIENTED_EDGE('',*,*,#8781,.F.);
#11695=ORIENTED_EDGE('',*,*,#8782,.F.);
#12386=CYLINDRICAL_SURFACE('',#16116,0.350000000000001);
#12387=CYLINDRICAL_SURFACE('',#16119,0.199999999999999);
#13132=ADVANCED_FACE('',(#2765,#1615),#2018,.F.);
#13133=ADVANCED_FACE('',(#2766),#12386,.T.);
#13134=ADVANCED_FACE('',(#2767),#2019,.T.);
#13135=ADVANCED_FACE('',(#2768),#12387,.T.);
#13136=ADVANCED_FACE('',(#2769),#2020,.F.);
#13348=CLOSED_SHELL('',(#13132,#13133,#13134,#13135,#13136));
#16112=AXIS2_PLACEMENT_3D('',#24163,#20228,#20229);
#16113=AXIS2_PLACEMENT_3D('',#24164,#20230,#20231);
#16114=AXIS2_PLACEMENT_3D('',#24166,#20232,#20233);
#16115=AXIS2_PLACEMENT_3D('',#24168,#20234,#20235);
#16116=AXIS2_PLACEMENT_3D('',#24169,#20236,#20237);
#16117=AXIS2_PLACEMENT_3D('',#24171,#20238,#20239);
#16118=AXIS2_PLACEMENT_3D('',#24173,#20241,#20242);
#16119=AXIS2_PLACEMENT_3D('',#24174,#20243,#20244);
#16120=AXIS2_PLACEMENT_3D('',#24177,#20246,#20247);
#16121=AXIS2_PLACEMENT_3D('',#24178,#20248,#20249);
#20228=DIRECTION('axis',(0.,0.,1.));
#20229=DIRECTION('refdir',(1.,0.,0.));
#20230=DIRECTION('center_axis',(0.,1.,0.));
#20231=DIRECTION('ref_axis',(1.,0.,0.));
#20232=DIRECTION('center_axis',(0.,1.,0.));
#20233=DIRECTION('ref_axis',(1.,0.,0.));
#20234=DIRECTION('center_axis',(0.,1.,0.));
#20235=DIRECTION('ref_axis',(1.,0.,0.));
#20236=DIRECTION('center_axis',(0.,1.,0.));
#20237=DIRECTION('ref_axis',(1.,0.,0.));
#20238=DIRECTION('center_axis',(0.,1.,0.));
#20239=DIRECTION('ref_axis',(1.,0.,0.));
#20240=DIRECTION('',(0.,-1.,0.));
#20241=DIRECTION('center_axis',(0.,1.,0.));
#20242=DIRECTION('ref_axis',(1.,0.,0.));
#20243=DIRECTION('center_axis',(0.,1.,0.));
#20244=DIRECTION('ref_axis',(1.,0.,0.));
#20245=DIRECTION('',(0.,-1.,0.));
#20246=DIRECTION('center_axis',(0.,1.,0.));
#20247=DIRECTION('ref_axis',(1.,0.,0.));
#20248=DIRECTION('center_axis',(0.,1.,0.));
#20249=DIRECTION('ref_axis',(1.,0.,0.));
#24163=CARTESIAN_POINT('',(0.,0.,0.));
#24164=CARTESIAN_POINT('Origin',(18.056769185842,8.3,6.69185245480489));
#24165=CARTESIAN_POINT('',(17.706769185842,8.3,6.69185245480489));
#24166=CARTESIAN_POINT('Origin',(18.056769185842,8.3,6.69185245480489));
#24167=CARTESIAN_POINT('',(17.856769185842,8.3,6.69185245480489));
#24168=CARTESIAN_POINT('Origin',(18.056769185842,8.3,6.69185245480489));
#24169=CARTESIAN_POINT('Origin',(18.056769185842,8.3,6.69185245480489));
#24170=CARTESIAN_POINT('',(17.706769185842,8.4,6.69185245480489));
#24171=CARTESIAN_POINT('Origin',(18.056769185842,8.4,6.69185245480489));
#24172=CARTESIAN_POINT('',(17.706769185842,8.3,6.69185245480489));
#24173=CARTESIAN_POINT('Origin',(18.056769185842,8.4,6.69185245480489));
#24174=CARTESIAN_POINT('Origin',(18.056769185842,7.6,6.69185245480489));
#24175=CARTESIAN_POINT('',(17.856769185842,7.6,6.69185245480489));
#24176=CARTESIAN_POINT('',(17.856769185842,7.6,6.69185245480489));
#24177=CARTESIAN_POINT('Origin',(18.056769185842,7.6,6.69185245480489));
#24178=CARTESIAN_POINT('Origin',(18.056769185842,7.6,6.69185245480489));
#24964=UNCERTAINTY_MEASURE_WITH_UNIT(LENGTH_MEASURE(0.001),#25101,
'DISTANCE_ACCURACY_VALUE',
'Maximum model space distance between geometric entities at asserted c
onnectivities');
#24979=UNCERTAINTY_MEASURE_WITH_UNIT(LENGTH_MEASURE(0.001),#25101,
'DISTANCE_ACCURACY_VALUE',
'Maximum model space distance between geometric entities at asserted c
onnectivities');
#25085=(
GEOMETRIC_REPRESENTATION_CONTEXT(3)
GLOBAL_UNCERTAINTY_ASSIGNED_CONTEXT((#24964))
GLOBAL_UNIT_ASSIGNED_CONTEXT((#25101,#25103,#25104))
REPRESENTATION_CONTEXT('','3D')
);
#25100=(
GEOMETRIC_REPRESENTATION_CONTEXT(3)
GLOBAL_UNCERTAINTY_ASSIGNED_CONTEXT((#24979))
GLOBAL_UNIT_ASSIGNED_CONTEXT((#25101,#25103,#25104))
REPRESENTATION_CONTEXT('','3D')
);
#25101=(
LENGTH_UNIT()
NAMED_UNIT(*)
SI_UNIT(.CENTI.,.METRE.)
);
#25103=(
NAMED_UNIT(*)
PLANE_ANGLE_UNIT()
SI_UNIT($,.RADIAN.)
);
#25104=(
NAMED_UNIT(*)
SI_UNIT($,.STERADIAN.)
SOLID_ANGLE_UNIT()
);
#25210=SHAPE_DEFINITION_REPRESENTATION(#25404,#25615);
#25404=PRODUCT_DEFINITION_SHAPE('',$,#25736);
#25615=SHAPE_REPRESENTATION('',(#16112),#25085);
#25630=PRODUCT_DEFINITION_CONTEXT('part definition',#25992,'design');
#25736=PRODUCT_DEFINITION('M4 low-profile retaining screw (14)',
'M4 low-profile retaining screw (14)',#25856,#25630);
#25856=PRODUCT_DEFINITION_FORMATION('',$,#26099);
#25992=APPLICATION_CONTEXT(
'Core Data for Automotive Mechanical Design Process');
#25993=PRODUCT_CONTEXT('part definition',#25992,'mechanical');
#26099=PRODUCT('M4 low-profile retaining screw (14)',
'M4 low-profile retaining screw (14)','M4 low-profile retaining screw (14)',
(#25993));
#26192=COLOUR_RGB('Black',0.12,0.14,0.17);
#26193=FILL_AREA_STYLE_COLOUR('',#26192);
#26194=FILL_AREA_STYLE('',(#26193));
#26195=SURFACE_STYLE_FILL_AREA(#26194);
#26196=SURFACE_SIDE_STYLE('',(#26195));
#26197=SURFACE_STYLE_USAGE(.BOTH.,#26196);
#26198=PRESENTATION_STYLE_ASSIGNMENT((#26197));
ENDSEC;
END-ISO-10303-21;
